ISO-10303-21;
HEADER;
/* Generated by software containing ST-Developer
 * from STEP Tools, Inc. (www.steptools.com) 
 */

FILE_DESCRIPTION(
/* description */ (''),
/* implementation_level */ '2;1');

FILE_NAME(
/* name */ '06_Ball_Bearing_6205-2RS.step',
/* time_stamp */ '2026-10-26T04:15:57-07:00',
/* author */ (''),
/* organization */ (''),
/* preprocessor_version */ 'ST-DEVELOPER v20.2',
/* originating_system */ 'Autodesk Translation Framework v15.15.0.0',
/* authorisation */ '');

FILE_SCHEMA (('AUTOMOTIVE_DESIGN { 1 0 10303 214 3 1 1 }'));
ENDSEC;

DATA;
#10=MECHANICAL_DESIGN_GEOMETRIC_PRESENTATION_REPRESENTATION('',(#457),#55737);
#366=CONICAL_SURFACE('',#29112,15.9,0.278299659005112);
#367=CONICAL_SURFACE('',#29117,22.7,0.278299659005112);
#368=CONICAL_SURFACE('',#29121,25.775,0.785398163397448);
#369=CONICAL_SURFACE('',#29125,25.775,0.785398163397448);
#370=CONICAL_SURFACE('',#29129,22.7,0.278299659005112);
#371=CONICAL_SURFACE('',#29133,15.9,0.278299659005112);
#372=CONICAL_SURFACE('',#29137,12.725,0.785398163397448);
#373=CONICAL_SURFACE('',#29141,12.725,0.785398163397448);
#417=SHAPE_REPRESENTATION_RELATIONSHIP('SRR','None',#55826,#437);
#437=ADVANCED_BREP_SHAPE_REPRESENTATION('',(#477),#55722);
#457=STYLED_ITEM('',(#55991),#477);
#477=MANIFOLD_SOLID_BREP('Body1',#27226);
#690=FACE_BOUND('',#9472,.T.);
#691=FACE_BOUND('',#9475,.T.);
#692=FACE_BOUND('',#9480,.T.);
#693=FACE_BOUND('',#9483,.T.);
#694=FACE_BOUND('',#9486,.T.);
#695=FACE_BOUND('',#9491,.T.);
#1381=PLANE('',#29115);
#1382=PLANE('',#29119);
#1383=PLANE('',#29127);
#1384=PLANE('',#29131);
#1385=PLANE('',#29135);
#1386=PLANE('',#29143);
#3316=LINE('',#45130,#5687);
#3317=LINE('',#45137,#5688);
#3318=LINE('',#45145,#5689);
#3319=LINE('',#45149,#5690);
#3320=LINE('',#45153,#5691);
#3321=LINE('',#45159,#5692);
#3322=LINE('',#45167,#5693);
#3323=LINE('',#45173,#5694);
#3324=LINE('',#45177,#5695);
#3325=LINE('',#45181,#5696);
#5687=VECTOR('',#34838,15.9);
#5688=VECTOR('',#34847,22.7);
#5689=VECTOR('',#34858,25.775);
#5690=VECTOR('',#34863,26.);
#5691=VECTOR('',#34868,25.775);
#5692=VECTOR('',#34875,22.7);
#5693=VECTOR('',#34886,15.9);
#5694=VECTOR('',#34893,12.725);
#5695=VECTOR('',#34898,12.5);
#5696=VECTOR('',#34903,12.725);
#6683=CYLINDRICAL_SURFACE('',#29123,26.);
#6684=CYLINDRICAL_SURFACE('',#29139,12.5);
#7815=FACE_OUTER_BOUND('',#9470,.T.);
#7816=FACE_OUTER_BOUND('',#9471,.T.);
#7817=FACE_OUTER_BOUND('',#9473,.T.);
#7818=FACE_OUTER_BOUND('',#9474,.T.);
#7819=FACE_OUTER_BOUND('',#9476,.T.);
#7820=FACE_OUTER_BOUND('',#9477,.T.);
#7821=FACE_OUTER_BOUND('',#9478,.T.);
#7822=FACE_OUTER_BOUND('',#9479,.T.);
#7823=FACE_OUTER_BOUND('',#9481,.T.);
#7824=FACE_OUTER_BOUND('',#9482,.T.);
#7825=FACE_OUTER_BOUND('',#9484,.T.);
#7826=FACE_OUTER_BOUND('',#9485,.T.);
#7827=FACE_OUTER_BOUND('',#9487,.T.);
#7828=FACE_OUTER_BOUND('',#9488,.T.);
#7829=FACE_OUTER_BOUND('',#9489,.T.);
#7830=FACE_OUTER_BOUND('',#9490,.T.);
#9470=EDGE_LOOP('',(#22874,#22875,#22876,#22877));
#9471=EDGE_LOOP('',(#22878));
#9472=EDGE_LOOP('',(#22879));
#9473=EDGE_LOOP('',(#22880,#22881,#22882,#22883));
#9474=EDGE_LOOP('',(#22884));
#9475=EDGE_LOOP('',(#22885));
#9476=EDGE_LOOP('',(#22886,#22887,#22888,#22889));
#9477=EDGE_LOOP('',(#22890,#22891,#22892,#22893));
#9478=EDGE_LOOP('',(#22894,#22895,#22896,#22897));
#9479=EDGE_LOOP('',(#22898));
#9480=EDGE_LOOP('',(#22899));
#9481=EDGE_LOOP('',(#22900,#22901,#22902,#22903));
#9482=EDGE_LOOP('',(#22904));
#9483=EDGE_LOOP('',(#22905));
#9484=EDGE_LOOP('',(#22906,#22907,#22908,#22909));
#9485=EDGE_LOOP('',(#22910));
#9486=EDGE_LOOP('',(#22911));
#9487=EDGE_LOOP('',(#22912,#22913,#22914,#22915));
#9488=EDGE_LOOP('',(#22916,#22917,#22918,#22919));
#9489=EDGE_LOOP('',(#22920,#22921,#22922,#22923));
#9490=EDGE_LOOP('',(#22924));
#9491=EDGE_LOOP('',(#22925));
#10740=CIRCLE('',#29113,16.);
#10741=CIRCLE('',#29114,15.8);
#10742=CIRCLE('',#29116,22.6);
#10743=CIRCLE('',#29118,22.8);
#10744=CIRCLE('',#29120,25.55);
#10745=CIRCLE('',#29122,26.);
#10746=CIRCLE('',#29124,26.);
#10747=CIRCLE('',#29126,25.55);
#10748=CIRCLE('',#29128,22.8);
#10749=CIRCLE('',#29130,22.6);
#10750=CIRCLE('',#29132,16.);
#10751=CIRCLE('',#29134,15.8);
#10752=CIRCLE('',#29136,12.95);
#10753=CIRCLE('',#29138,12.5);
#10754=CIRCLE('',#29140,12.5);
#10755=CIRCLE('',#29142,12.95);
#13051=VERTEX_POINT('',#45127);
#13052=VERTEX_POINT('',#45129);
#13053=VERTEX_POINT('',#45133);
#13054=VERTEX_POINT('',#45136);
#13055=VERTEX_POINT('',#45140);
#13056=VERTEX_POINT('',#45143);
#13057=VERTEX_POINT('',#45147);
#13058=VERTEX_POINT('',#45151);
#13059=VERTEX_POINT('',#45155);
#13060=VERTEX_POINT('',#45158);
#13061=VERTEX_POINT('',#45162);
#13062=VERTEX_POINT('',#45165);
#13063=VERTEX_POINT('',#45169);
#13064=VERTEX_POINT('',#45172);
#13065=VERTEX_POINT('',#45176);
#13066=VERTEX_POINT('',#45180);
#16441=EDGE_CURVE('',#13051,#13051,#10740,.T.);
#16442=EDGE_CURVE('',#13051,#13052,#3316,.T.);
#16443=EDGE_CURVE('',#13052,#13052,#10741,.T.);
#16444=EDGE_CURVE('',#13053,#13053,#10742,.T.);
#16445=EDGE_CURVE('',#13053,#13054,#3317,.T.);
#16446=EDGE_CURVE('',#13054,#13054,#10743,.T.);
#16447=EDGE_CURVE('',#13055,#13055,#10744,.T.);
#16448=EDGE_CURVE('',#13056,#13056,#10745,.T.);
#16449=EDGE_CURVE('',#13056,#13055,#3318,.T.);
#16450=EDGE_CURVE('',#13057,#13057,#10746,.T.);
#16451=EDGE_CURVE('',#13057,#13056,#3319,.T.);
#16452=EDGE_CURVE('',#13058,#13058,#10747,.T.);
#16453=EDGE_CURVE('',#13058,#13057,#3320,.T.);
#16454=EDGE_CURVE('',#13059,#13059,#10748,.T.);
#16455=EDGE_CURVE('',#13059,#13060,#3321,.T.);
#16456=EDGE_CURVE('',#13060,#13060,#10749,.T.);
#16457=EDGE_CURVE('',#13061,#13061,#10750,.T.);
#16458=EDGE_CURVE('',#13062,#13062,#10751,.T.);
#16459=EDGE_CURVE('',#13062,#13061,#3322,.T.);
#16460=EDGE_CURVE('',#13063,#13063,#10752,.T.);
#16461=EDGE_CURVE('',#13063,#13064,#3323,.T.);
#16462=EDGE_CURVE('',#13064,#13064,#10753,.T.);
#16463=EDGE_CURVE('',#13064,#13065,#3324,.T.);
#16464=EDGE_CURVE('',#13065,#13065,#10754,.T.);
#16465=EDGE_CURVE('',#13065,#13066,#3325,.T.);
#16466=EDGE_CURVE('',#13066,#13066,#10755,.T.);
#22874=ORIENTED_EDGE('',*,*,#16441,.F.);
#22875=ORIENTED_EDGE('',*,*,#16442,.T.);
#22876=ORIENTED_EDGE('',*,*,#16443,.T.);
#22877=ORIENTED_EDGE('',*,*,#16442,.F.);
#22878=ORIENTED_EDGE('',*,*,#16444,.F.);
#22879=ORIENTED_EDGE('',*,*,#16441,.T.);
#22880=ORIENTED_EDGE('',*,*,#16444,.T.);
#22881=ORIENTED_EDGE('',*,*,#16445,.T.);
#22882=ORIENTED_EDGE('',*,*,#16446,.F.);
#22883=ORIENTED_EDGE('',*,*,#16445,.F.);
#22884=ORIENTED_EDGE('',*,*,#16447,.F.);
#22885=ORIENTED_EDGE('',*,*,#16446,.T.);
#22886=ORIENTED_EDGE('',*,*,#16448,.F.);
#22887=ORIENTED_EDGE('',*,*,#16449,.T.);
#22888=ORIENTED_EDGE('',*,*,#16447,.T.);
#22889=ORIENTED_EDGE('',*,*,#16449,.F.);
#22890=ORIENTED_EDGE('',*,*,#16450,.F.);
#22891=ORIENTED_EDGE('',*,*,#16451,.T.);
#22892=ORIENTED_EDGE('',*,*,#16448,.T.);
#22893=ORIENTED_EDGE('',*,*,#16451,.F.);
#22894=ORIENTED_EDGE('',*,*,#16452,.F.);
#22895=ORIENTED_EDGE('',*,*,#16453,.T.);
#22896=ORIENTED_EDGE('',*,*,#16450,.T.);
#22897=ORIENTED_EDGE('',*,*,#16453,.F.);
#22898=ORIENTED_EDGE('',*,*,#16452,.T.);
#22899=ORIENTED_EDGE('',*,*,#16454,.F.);
#22900=ORIENTED_EDGE('',*,*,#16454,.T.);
#22901=ORIENTED_EDGE('',*,*,#16455,.T.);
#22902=ORIENTED_EDGE('',*,*,#16456,.F.);
#22903=ORIENTED_EDGE('',*,*,#16455,.F.);
#22904=ORIENTED_EDGE('',*,*,#16456,.T.);
#22905=ORIENTED_EDGE('',*,*,#16457,.F.);
#22906=ORIENTED_EDGE('',*,*,#16458,.F.);
#22907=ORIENTED_EDGE('',*,*,#16459,.T.);
#22908=ORIENTED_EDGE('',*,*,#16457,.T.);
#22909=ORIENTED_EDGE('',*,*,#16459,.F.);
#22910=ORIENTED_EDGE('',*,*,#16458,.T.);
#22911=ORIENTED_EDGE('',*,*,#16460,.F.);
#22912=ORIENTED_EDGE('',*,*,#16460,.T.);
#22913=ORIENTED_EDGE('',*,*,#16461,.T.);
#22914=ORIENTED_EDGE('',*,*,#16462,.F.);
#22915=ORIENTED_EDGE('',*,*,#16461,.F.);
#22916=ORIENTED_EDGE('',*,*,#16462,.T.);
#22917=ORIENTED_EDGE('',*,*,#16463,.T.);
#22918=ORIENTED_EDGE('',*,*,#16464,.F.);
#22919=ORIENTED_EDGE('',*,*,#16463,.F.);
#22920=ORIENTED_EDGE('',*,*,#16464,.T.);
#22921=ORIENTED_EDGE('',*,*,#16465,.T.);
#22922=ORIENTED_EDGE('',*,*,#16466,.F.);
#22923=ORIENTED_EDGE('',*,*,#16465,.F.);
#22924=ORIENTED_EDGE('',*,*,#16443,.F.);
#22925=ORIENTED_EDGE('',*,*,#16466,.T.);
#26639=ADVANCED_FACE('',(#7815),#366,.T.);
#26640=ADVANCED_FACE('',(#7816,#690),#1381,.T.);
#26641=ADVANCED_FACE('',(#7817),#367,.F.);
#26642=ADVANCED_FACE('',(#7818,#691),#1382,.T.);
#26643=ADVANCED_FACE('',(#7819),#368,.T.);
#26644=ADVANCED_FACE('',(#7820),#6683,.T.);
#26645=ADVANCED_FACE('',(#7821),#369,.T.);
#26646=ADVANCED_FACE('',(#7822,#692),#1383,.T.);
#26647=ADVANCED_FACE('',(#7823),#370,.F.);
#26648=ADVANCED_FACE('',(#7824,#693),#1384,.T.);
#26649=ADVANCED_FACE('',(#7825),#371,.T.);
#26650=ADVANCED_FACE('',(#7826,#694),#1385,.T.);
#26651=ADVANCED_FACE('',(#7827),#372,.F.);
#26652=ADVANCED_FACE('',(#7828),#6684,.F.);
#26653=ADVANCED_FACE('',(#7829),#373,.F.);
#26654=ADVANCED_FACE('',(#7830,#695),#1386,.T.);
#27226=CLOSED_SHELL('',(#26639,#26640,#26641,#26642,#26643,#26644,#26645,
#26646,#26647,#26648,#26649,#26650,#26651,#26652,#26653,#26654));
#29111=AXIS2_PLACEMENT_3D('',#45125,#34832,#34833);
#29112=AXIS2_PLACEMENT_3D('',#45126,#34834,#34835);
#29113=AXIS2_PLACEMENT_3D('',#45128,#34836,#34837);
#29114=AXIS2_PLACEMENT_3D('',#45131,#34839,#34840);
#29115=AXIS2_PLACEMENT_3D('',#45132,#34841,#34842);
#29116=AXIS2_PLACEMENT_3D('',#45134,#34843,#34844);
#29117=AXIS2_PLACEMENT_3D('',#45135,#34845,#34846);
#29118=AXIS2_PLACEMENT_3D('',#45138,#34848,#34849);
#29119=AXIS2_PLACEMENT_3D('',#45139,#34850,#34851);
#29120=AXIS2_PLACEMENT_3D('',#45141,#34852,#34853);
#29121=AXIS2_PLACEMENT_3D('',#45142,#34854,#34855);
#29122=AXIS2_PLACEMENT_3D('',#45144,#34856,#34857);
#29123=AXIS2_PLACEMENT_3D('',#45146,#34859,#34860);
#29124=AXIS2_PLACEMENT_3D('',#45148,#34861,#34862);
#29125=AXIS2_PLACEMENT_3D('',#45150,#34864,#34865);
#29126=AXIS2_PLACEMENT_3D('',#45152,#34866,#34867);
#29127=AXIS2_PLACEMENT_3D('',#45154,#34869,#34870);
#29128=AXIS2_PLACEMENT_3D('',#45156,#34871,#34872);
#29129=AXIS2_PLACEMENT_3D('',#45157,#34873,#34874);
#29130=AXIS2_PLACEMENT_3D('',#45160,#34876,#34877);
#29131=AXIS2_PLACEMENT_3D('',#45161,#34878,#34879);
#29132=AXIS2_PLACEMENT_3D('',#45163,#34880,#34881);
#29133=AXIS2_PLACEMENT_3D('',#45164,#34882,#34883);
#29134=AXIS2_PLACEMENT_3D('',#45166,#34884,#34885);
#29135=AXIS2_PLACEMENT_3D('',#45168,#34887,#34888);
#29136=AXIS2_PLACEMENT_3D('',#45170,#34889,#34890);
#29137=AXIS2_PLACEMENT_3D('',#45171,#34891,#34892);
#29138=AXIS2_PLACEMENT_3D('',#45174,#34894,#34895);
#29139=AXIS2_PLACEMENT_3D('',#45175,#34896,#34897);
#29140=AXIS2_PLACEMENT_3D('',#45178,#34899,#34900);
#29141=AXIS2_PLACEMENT_3D('',#45179,#34901,#34902);
#29142=AXIS2_PLACEMENT_3D('',#45182,#34904,#34905);
#29143=AXIS2_PLACEMENT_3D('',#45183,#34906,#34907);
#34832=DIRECTION('axis',(0.,0.,1.));
#34833=DIRECTION('refdir',(1.,0.,0.));
#34834=DIRECTION('center_axis',(1.,0.,0.));
#34835=DIRECTION('ref_axis',(0.,1.,0.));
#34836=DIRECTION('center_axis',(1.,0.,0.));
#34837=DIRECTION('ref_axis',(0.,0.,-1.));
#34838=DIRECTION('',(-0.961523947640823,0.274721127897378,3.36436349937675E-17));
#34839=DIRECTION('center_axis',(1.,0.,0.));
#34840=DIRECTION('ref_axis',(0.,0.,-1.));
#34841=DIRECTION('center_axis',(-1.,0.,0.));
#34842=DIRECTION('ref_axis',(0.,0.,1.));
#34843=DIRECTION('center_axis',(1.,0.,0.));
#34844=DIRECTION('ref_axis',(0.,0.,-1.));
#34845=DIRECTION('center_axis',(-1.,0.,0.));
#34846=DIRECTION('ref_axis',(0.,1.,0.));
#34847=DIRECTION('',(-0.961523947640823,-0.274721127897378,-3.36436349937675E-17));
#34848=DIRECTION('center_axis',(1.,0.,0.));
#34849=DIRECTION('ref_axis',(0.,0.,-1.));
#34850=DIRECTION('center_axis',(-1.,0.,0.));
#34851=DIRECTION('ref_axis',(0.,0.,1.));
#34852=DIRECTION('center_axis',(1.,0.,0.));
#34853=DIRECTION('ref_axis',(0.,0.,-1.));
#34854=DIRECTION('center_axis',(1.,0.,0.));
#34855=DIRECTION('ref_axis',(0.,1.,0.));
#34856=DIRECTION('center_axis',(1.,0.,0.));
#34857=DIRECTION('ref_axis',(0.,0.,-1.));
#34858=DIRECTION('',(-0.707106781186548,0.707106781186547,8.65956056235493E-17));
#34859=DIRECTION('center_axis',(1.,0.,0.));
#34860=DIRECTION('ref_axis',(0.,1.,0.));
#34861=DIRECTION('center_axis',(1.,0.,0.));
#34862=DIRECTION('ref_axis',(0.,0.,-1.));
#34863=DIRECTION('',(-1.,0.,0.));
#34864=DIRECTION('center_axis',(-1.,0.,0.));
#34865=DIRECTION('ref_axis',(0.,1.,0.));
#34866=DIRECTION('center_axis',(1.,0.,0.));
#34867=DIRECTION('ref_axis',(0.,0.,-1.));
#34868=DIRECTION('',(-0.707106781186547,-0.707106781186547,-8.65956056235493E-17));
#34869=DIRECTION('center_axis',(1.,0.,0.));
#34870=DIRECTION('ref_axis',(0.,0.,-1.));
#34871=DIRECTION('center_axis',(1.,0.,0.));
#34872=DIRECTION('ref_axis',(0.,0.,-1.));
#34873=DIRECTION('center_axis',(1.,0.,0.));
#34874=DIRECTION('ref_axis',(0.,1.,0.));
#34875=DIRECTION('',(-0.961523947640823,0.274721127897379,3.36436349937676E-17));
#34876=DIRECTION('center_axis',(1.,0.,0.));
#34877=DIRECTION('ref_axis',(0.,0.,-1.));
#34878=DIRECTION('center_axis',(1.,0.,0.));
#34879=DIRECTION('ref_axis',(0.,0.,-1.));
#34880=DIRECTION('center_axis',(1.,0.,0.));
#34881=DIRECTION('ref_axis',(0.,0.,-1.));
#34882=DIRECTION('center_axis',(-1.,0.,0.));
#34883=DIRECTION('ref_axis',(0.,1.,0.));
#34884=DIRECTION('center_axis',(1.,0.,0.));
#34885=DIRECTION('ref_axis',(0.,0.,-1.));
#34886=DIRECTION('',(-0.961523947640823,-0.274721127897379,-3.36436349937676E-17));
#34887=DIRECTION('center_axis',(1.,0.,0.));
#34888=DIRECTION('ref_axis',(0.,0.,-1.));
#34889=DIRECTION('center_axis',(1.,0.,0.));
#34890=DIRECTION('ref_axis',(0.,0.,-1.));
#34891=DIRECTION('center_axis',(1.,0.,0.));
#34892=DIRECTION('ref_axis',(0.,1.,0.));
#34893=DIRECTION('',(-0.707106781186547,0.707106781186547,8.65956056235493E-17));
#34894=DIRECTION('center_axis',(1.,0.,0.));
#34895=DIRECTION('ref_axis',(0.,0.,-1.));
#34896=DIRECTION('center_axis',(1.,0.,0.));
#34897=DIRECTION('ref_axis',(0.,1.,0.));
#34898=DIRECTION('',(-1.,0.,0.));
#34899=DIRECTION('center_axis',(1.,0.,0.));
#34900=DIRECTION('ref_axis',(0.,0.,-1.));
#34901=DIRECTION('center_axis',(-1.,0.,0.));
#34902=DIRECTION('ref_axis',(0.,1.,0.));
#34903=DIRECTION('',(-0.707106781186548,-0.707106781186547,-8.65956056235493E-17));
#34904=DIRECTION('center_axis',(1.,0.,0.));
#34905=DIRECTION('ref_axis',(0.,0.,-1.));
#34906=DIRECTION('center_axis',(-1.,0.,0.));
#34907=DIRECTION('ref_axis',(0.,0.,1.));
#45125=CARTESIAN_POINT('',(0.,0.,0.));
#45126=CARTESIAN_POINT('Origin',(0.35,0.,0.));
#45127=CARTESIAN_POINT('',(0.7,-16.,-1.95943487863577E-15));
#45128=CARTESIAN_POINT('Origin',(0.7,0.,0.));
#45129=CARTESIAN_POINT('',(-3.46944695195361E-16,-15.8,-1.93494194265282E-15));
#45130=CARTESIAN_POINT('',(0.35,-15.9,-1.94718841064429E-15));
#45131=CARTESIAN_POINT('Origin',(0.,0.,0.));
#45132=CARTESIAN_POINT('Origin',(0.7,22.6,0.));
#45133=CARTESIAN_POINT('',(0.700000000000001,-22.6,-2.76770176607302E-15));
#45134=CARTESIAN_POINT('Origin',(0.7,0.,0.));
#45135=CARTESIAN_POINT('Origin',(0.35,0.,0.));
#45136=CARTESIAN_POINT('',(3.46944695195361E-16,-22.8,-2.79219470205597E-15));
#45137=CARTESIAN_POINT('',(0.35,-22.7,-2.77994823406449E-15));
#45138=CARTESIAN_POINT('Origin',(0.,0.,0.));
#45139=CARTESIAN_POINT('Origin',(0.,25.55,0.));
#45140=CARTESIAN_POINT('',(-4.5102810375397E-16,-25.55,-3.12897257182149E-15));
#45141=CARTESIAN_POINT('Origin',(0.,0.,0.));
#45142=CARTESIAN_POINT('Origin',(0.225,0.,0.));
#45143=CARTESIAN_POINT('',(0.45,-26.,-3.18408167778312E-15));
#45144=CARTESIAN_POINT('Origin',(0.45,0.,0.));
#45145=CARTESIAN_POINT('',(0.225,-25.775,-3.1565271248023E-15));
#45146=CARTESIAN_POINT('Origin',(7.5,0.,0.));
#45147=CARTESIAN_POINT('',(14.55,-26.,-3.18408167778312E-15));
#45148=CARTESIAN_POINT('Origin',(14.55,0.,0.));
#45149=CARTESIAN_POINT('',(7.5,-26.,-3.18408167778312E-15));
#45150=CARTESIAN_POINT('Origin',(14.775,0.,0.));
#45151=CARTESIAN_POINT('',(15.,-25.55,-3.12897257182149E-15));
#45152=CARTESIAN_POINT('Origin',(15.,0.,0.));
#45153=CARTESIAN_POINT('',(14.775,-25.775,-3.1565271248023E-15));
#45154=CARTESIAN_POINT('Origin',(15.,22.8,0.));
#45155=CARTESIAN_POINT('',(15.,-22.8,-2.79219470205597E-15));
#45156=CARTESIAN_POINT('Origin',(15.,0.,0.));
#45157=CARTESIAN_POINT('Origin',(14.65,0.,0.));
#45158=CARTESIAN_POINT('',(14.3,-22.6,-2.76770176607302E-15));
#45159=CARTESIAN_POINT('',(14.65,-22.7,-2.77994823406449E-15));
#45160=CARTESIAN_POINT('Origin',(14.3,0.,0.));
#45161=CARTESIAN_POINT('Origin',(14.3,16.,0.));
#45162=CARTESIAN_POINT('',(14.3,-16.,-1.95943487863577E-15));
#45163=CARTESIAN_POINT('Origin',(14.3,0.,0.));
#45164=CARTESIAN_POINT('Origin',(14.65,0.,0.));
#45165=CARTESIAN_POINT('',(15.,-15.8,-1.93494194265282E-15));
#45166=CARTESIAN_POINT('Origin',(15.,0.,0.));
#45167=CARTESIAN_POINT('',(14.65,-15.9,-1.94718841064429E-15));
#45168=CARTESIAN_POINT('Origin',(15.,12.95,0.));
#45169=CARTESIAN_POINT('',(15.,-12.95,-1.58591760489582E-15));
#45170=CARTESIAN_POINT('Origin',(15.,0.,0.));
#45171=CARTESIAN_POINT('Origin',(14.775,0.,0.));
#45172=CARTESIAN_POINT('',(14.55,-12.5,-1.53080849893419E-15));
#45173=CARTESIAN_POINT('',(14.775,-12.725,-1.55836305191501E-15));
#45174=CARTESIAN_POINT('Origin',(14.55,0.,0.));
#45175=CARTESIAN_POINT('Origin',(7.5,0.,0.));
#45176=CARTESIAN_POINT('',(0.45,-12.5,-1.53080849893419E-15));
#45177=CARTESIAN_POINT('',(7.5,-12.5,-1.53080849893419E-15));
#45178=CARTESIAN_POINT('Origin',(0.45,0.,0.));
#45179=CARTESIAN_POINT('Origin',(0.225,0.,0.));
#45180=CARTESIAN_POINT('',(-2.08166817117217E-16,-12.95,-1.58591760489582E-15));
#45181=CARTESIAN_POINT('',(0.225,-12.725,-1.55836305191501E-15));
#45182=CARTESIAN_POINT('Origin',(0.,0.,0.));
#45183=CARTESIAN_POINT('Origin',(0.,15.8,0.));
#55700=UNCERTAINTY_MEASURE_WITH_UNIT(LENGTH_MEASURE(0.01),#55738,
'DISTANCE_ACCURACY_VALUE',
'Maximum model space distance between geometric entities at asserted c
onnectivities');
#55715=UNCERTAINTY_MEASURE_WITH_UNIT(LENGTH_MEASURE(0.01),#55738,
'DISTANCE_ACCURACY_VALUE',
'Maximum model space distance between geometric entities at asserted c
onnectivities');
#55722=(
GEOMETRIC_REPRESENTATION_CONTEXT(3)
GLOBAL_UNCERTAINTY_ASSIGNED_CONTEXT((#55700))
GLOBAL_UNIT_ASSIGNED_CONTEXT((#55738,#55740,#55741))
REPRESENTATION_CONTEXT('','3D')
);
#55737=(
GEOMETRIC_REPRESENTATION_CONTEXT(3)
GLOBAL_UNCERTAINTY_ASSIGNED_CONTEXT((#55715))
GLOBAL_UNIT_ASSIGNED_CONTEXT((#55738,#55740,#55741))
REPRESENTATION_CONTEXT('','3D')
);
#55738=(
LENGTH_UNIT()
NAMED_UNIT(*)
SI_UNIT(.MILLI.,.METRE.)
);
#55740=(
NAMED_UNIT(*)
PLANE_ANGLE_UNIT()
SI_UNIT($,.RADIAN.)
);
#55741=(
NAMED_UNIT(*)
SI_UNIT($,.STERADIAN.)
SOLID_ANGLE_UNIT()
);
#55748=SHAPE_DEFINITION_REPRESENTATION(#55769,#55826);
#55769=PRODUCT_DEFINITION_SHAPE('',$,#55848);
#55826=SHAPE_REPRESENTATION('',(#29111),#55722);
#55841=PRODUCT_DEFINITION_CONTEXT('part definition',#55906,'design');
#55848=PRODUCT_DEFINITION('2026-10-26-00-34-22-718',
'06_Ball_Bearing_6205-2RS',#55869,#55841);
#55869=PRODUCT_DEFINITION_FORMATION('',$,#55914);
#55906=APPLICATION_CONTEXT(
'Core Data for Automotive Mechanical Design Process');
#55907=PRODUCT_CONTEXT('part definition',#55906,'mechanical');
#55914=PRODUCT('2026-10-26-00-34-22-718','06_Ball_Bearing_6205-2RS',$,(#55907));
#55985=COLOUR_RGB('Grey',0.48,0.52,0.57);
#55986=FILL_AREA_STYLE_COLOUR('',#55985);
#55987=FILL_AREA_STYLE('',(#55986));
#55988=SURFACE_STYLE_FILL_AREA(#55987);
#55989=SURFACE_SIDE_STYLE('',(#55988));
#55990=SURFACE_STYLE_USAGE(.BOTH.,#55989);
#55991=PRESENTATION_STYLE_ASSIGNMENT((#55990));
ENDSEC;
END-ISO-10303-21;
